ISO-10303-21;
HEADER;
/* Generated by software containing ST-Developer
 * from STEP Tools, Inc. (www.steptools.com) 
 */

FILE_DESCRIPTION(
/* description */ (''),
/* implementation_level */ '2;1');

FILE_NAME(
/* name */ 'Base Lock Knob Lever (stainless, bent).step',
/* time_stamp */ '2026-10-05T09:57:53+05:00',
/* author */ (''),
/* organization */ (''),
/* preprocessor_version */ 'ST-DEVELOPER v20.2',
/* originating_system */ 'Autodesk Translation Framework v15.15.0.0',
/* authorisation */ '');

FILE_SCHEMA (('AUTOMOTIVE_DESIGN { 1 0 10303 214 3 1 1 }'));
ENDSEC;

DATA;
#10=MECHANICAL_DESIGN_GEOMETRIC_PRESENTATION_REPRESENTATION('',(#559),#113984);
#523=SHAPE_REPRESENTATION_RELATIONSHIP('SRR','None',#114060,#541);
#541=ADVANCED_BREP_SHAPE_REPRESENTATION('',(#577),#113974);
#559=STYLED_ITEM('',(#114289),#577);
#577=MANIFOLD_SOLID_BREP('Base Lock Knob Lever (stainless, bent)',#60400);
#601=ELLIPSE('',#62936,0.751653400711626,0.5);
#602=ELLIPSE('',#62946,0.751653400711626,0.5);
#707=CYLINDRICAL_SURFACE('',#62924,0.5);
#708=CYLINDRICAL_SURFACE('',#62927,5.);
#709=CYLINDRICAL_SURFACE('',#62930,0.5);
#710=CYLINDRICAL_SURFACE('',#62934,0.5);
#711=CYLINDRICAL_SURFACE('',#62939,0.5);
#712=CYLINDRICAL_SURFACE('',#62945,0.5);
#713=CYLINDRICAL_SURFACE('',#62953,2.15);
#1254=CIRCLE('',#62925,0.5);
#1255=CIRCLE('',#62926,0.5);
#1256=CIRCLE('',#62928,5.);
#1257=CIRCLE('',#62929,5.);
#1258=CIRCLE('',#62931,0.5);
#1259=CIRCLE('',#62932,0.5);
#1260=CIRCLE('',#62935,0.5);
#1261=CIRCLE('',#62940,0.5);
#1262=CIRCLE('',#62941,0.5);
#1263=CIRCLE('',#62943,0.5);
#1264=CIRCLE('',#62944,2.15);
#1265=CIRCLE('',#62954,2.15);
#1847=FACE_BOUND('',#10330,.T.);
#1848=FACE_BOUND('',#10341,.T.);
#3696=PLANE('',#62933);
#3697=PLANE('',#62937);
#3698=PLANE('',#62938);
#3699=PLANE('',#62942);
#3700=PLANE('',#62947);
#3701=PLANE('',#62948);
#3702=PLANE('',#62949);
#3703=PLANE('',#62950);
#3704=PLANE('',#62951);
#3705=PLANE('',#62952);
#3706=PLANE('',#62955);
#3707=PLANE('',#62956);
#6749=FACE_OUTER_BOUND('',#10321,.T.);
#6750=FACE_OUTER_BOUND('',#10322,.T.);
#6751=FACE_OUTER_BOUND('',#10323,.T.);
#6752=FACE_OUTER_BOUND('',#10324,.T.);
#6753=FACE_OUTER_BOUND('',#10325,.T.);
#6754=FACE_OUTER_BOUND('',#10326,.T.);
#6755=FACE_OUTER_BOUND('',#10327,.T.);
#6756=FACE_OUTER_BOUND('',#10328,.T.);
#6757=FACE_OUTER_BOUND('',#10329,.T.);
#6758=FACE_OUTER_BOUND('',#10331,.T.);
#6759=FACE_OUTER_BOUND('',#10332,.T.);
#6760=FACE_OUTER_BOUND('',#10333,.T.);
#6761=FACE_OUTER_BOUND('',#10334,.T.);
#6762=FACE_OUTER_BOUND('',#10335,.T.);
#6763=FACE_OUTER_BOUND('',#10336,.T.);
#6764=FACE_OUTER_BOUND('',#10337,.T.);
#6765=FACE_OUTER_BOUND('',#10338,.T.);
#6766=FACE_OUTER_BOUND('',#10339,.T.);
#6767=FACE_OUTER_BOUND('',#10340,.T.);
#10321=EDGE_LOOP('',(#53501,#53502,#53503,#53504));
#10322=EDGE_LOOP('',(#53505,#53506,#53507,#53508));
#10323=EDGE_LOOP('',(#53509,#53510,#53511,#53512));
#10324=EDGE_LOOP('',(#53513,#53514,#53515,#53516,#53517,#53518));
#10325=EDGE_LOOP('',(#53519,#53520,#53521,#53522));
#10326=EDGE_LOOP('',(#53523,#53524,#53525,#53526));
#10327=EDGE_LOOP('',(#53527,#53528,#53529,#53530,#53531,#53532,#53533));
#10328=EDGE_LOOP('',(#53534,#53535,#53536,#53537));
#10329=EDGE_LOOP('',(#53538,#53539,#53540,#53541,#53542,#53543,#53544,#53545,
#53546,#53547,#53548));
#10330=EDGE_LOOP('',(#53549));
#10331=EDGE_LOOP('',(#53550,#53551,#53552,#53553));
#10332=EDGE_LOOP('',(#53554,#53555,#53556,#53557,#53558,#53559));
#10333=EDGE_LOOP('',(#53560,#53561,#53562,#53563));
#10334=EDGE_LOOP('',(#53564,#53565,#53566,#53567,#53568,#53569,#53570,#53571,
#53572));
#10335=EDGE_LOOP('',(#53573,#53574,#53575,#53576));
#10336=EDGE_LOOP('',(#53577,#53578,#53579,#53580,#53581));
#10337=EDGE_LOOP('',(#53582,#53583,#53584,#53585));
#10338=EDGE_LOOP('',(#53586,#53587,#53588,#53589));
#10339=EDGE_LOOP('',(#53590,#53591,#53592,#53593));
#10340=EDGE_LOOP('',(#53594,#53595,#53596,#53597,#53598,#53599,#53600,#53601));
#10341=EDGE_LOOP('',(#53602));
#16161=LINE('',#102024,#22195);
#16162=LINE('',#102027,#22196);
#16163=LINE('',#102032,#22197);
#16164=LINE('',#102038,#22198);
#16165=LINE('',#102042,#22199);
#16166=LINE('',#102044,#22200);
#16167=LINE('',#102046,#22201);
#16168=LINE('',#102048,#22202);
#16169=LINE('',#102049,#22203);
#16170=LINE('',#102055,#22204);
#16171=LINE('',#102058,#22205);
#16172=LINE('',#102060,#22206);
#16173=LINE('',#102061,#22207);
#16174=LINE('',#102064,#22208);
#16175=LINE('',#102066,#22209);
#16176=LINE('',#102068,#22210);
#16177=LINE('',#102070,#22211);
#16178=LINE('',#102072,#22212);
#16179=LINE('',#102073,#22213);
#16180=LINE('',#102079,#22214);
#16181=LINE('',#102082,#22215);
#16182=LINE('',#102084,#22216);
#16183=LINE('',#102086,#22217);
#16184=LINE('',#102092,#22218);
#16185=LINE('',#102095,#22219);
#16186=LINE('',#102097,#22220);
#16187=LINE('',#102099,#22221);
#16188=LINE('',#102100,#22222);
#16189=LINE('',#102103,#22223);
#16190=LINE('',#102104,#22224);
#16191=LINE('',#102107,#22225);
#16192=LINE('',#102109,#22226);
#16193=LINE('',#102110,#22227);
#16194=LINE('',#102112,#22228);
#16195=LINE('',#102113,#22229);
#16196=LINE('',#102118,#22230);
#16197=LINE('',#102121,#22231);
#22195=VECTOR('',#73695,10.);
#22196=VECTOR('',#73698,10.);
#22197=VECTOR('',#73703,10.);
#22198=VECTOR('',#73710,10.);
#22199=VECTOR('',#73715,10.);
#22200=VECTOR('',#73716,10.);
#22201=VECTOR('',#73717,10.);
#22202=VECTOR('',#73718,10.);
#22203=VECTOR('',#73719,10.);
#22204=VECTOR('',#73726,10.);
#22205=VECTOR('',#73729,10.);
#22206=VECTOR('',#73730,10.);
#22207=VECTOR('',#73731,10.);
#22208=VECTOR('',#73734,10.);
#22209=VECTOR('',#73735,10.);
#22210=VECTOR('',#73736,10.);
#22211=VECTOR('',#73737,10.);
#22212=VECTOR('',#73738,10.);
#22213=VECTOR('',#73739,10.);
#22214=VECTOR('',#73746,10.);
#22215=VECTOR('',#73749,10.);
#22216=VECTOR('',#73750,10.);
#22217=VECTOR('',#73753,10.);
#22218=VECTOR('',#73760,10.);
#22219=VECTOR('',#73763,10.);
#22220=VECTOR('',#73764,10.);
#22221=VECTOR('',#73765,10.);
#22222=VECTOR('',#73766,10.);
#22223=VECTOR('',#73769,10.);
#22224=VECTOR('',#73770,10.);
#22225=VECTOR('',#73773,10.);
#22226=VECTOR('',#73774,10.);
#22227=VECTOR('',#73775,10.);
#22228=VECTOR('',#73778,10.);
#22229=VECTOR('',#73779,10.);
#22230=VECTOR('',#73786,2.15);
#22231=VECTOR('',#73791,10.);
#29413=VERTEX_POINT('',#102020);
#29414=VERTEX_POINT('',#102021);
#29415=VERTEX_POINT('',#102023);
#29416=VERTEX_POINT('',#102025);
#29417=VERTEX_POINT('',#102029);
#29418=VERTEX_POINT('',#102031);
#29419=VERTEX_POINT('',#102035);
#29420=VERTEX_POINT('',#102037);
#29421=VERTEX_POINT('',#102041);
#29422=VERTEX_POINT('',#102043);
#29423=VERTEX_POINT('',#102045);
#29424=VERTEX_POINT('',#102047);
#29425=VERTEX_POINT('',#102051);
#29426=VERTEX_POINT('',#102053);
#29427=VERTEX_POINT('',#102057);
#29428=VERTEX_POINT('',#102059);
#29429=VERTEX_POINT('',#102063);
#29430=VERTEX_POINT('',#102065);
#29431=VERTEX_POINT('',#102067);
#29432=VERTEX_POINT('',#102069);
#29433=VERTEX_POINT('',#102071);
#29434=VERTEX_POINT('',#102075);
#29435=VERTEX_POINT('',#102077);
#29436=VERTEX_POINT('',#102081);
#29437=VERTEX_POINT('',#102083);
#29438=VERTEX_POINT('',#102087);
#29439=VERTEX_POINT('',#102090);
#29440=VERTEX_POINT('',#102094);
#29441=VERTEX_POINT('',#102096);
#29442=VERTEX_POINT('',#102098);
#29443=VERTEX_POINT('',#102102);
#29444=VERTEX_POINT('',#102106);
#29445=VERTEX_POINT('',#102108);
#29446=VERTEX_POINT('',#102117);
#37583=EDGE_CURVE('',#29413,#29414,#1254,.T.);
#37584=EDGE_CURVE('',#29414,#29415,#16161,.T.);
#37585=EDGE_CURVE('',#29415,#29416,#1255,.T.);
#37586=EDGE_CURVE('',#29416,#29413,#16162,.T.);
#37587=EDGE_CURVE('',#29414,#29417,#1256,.T.);
#37588=EDGE_CURVE('',#29418,#29417,#16163,.T.);
#37589=EDGE_CURVE('',#29415,#29418,#1257,.T.);
#37590=EDGE_CURVE('',#29417,#29419,#1258,.T.);
#37591=EDGE_CURVE('',#29419,#29420,#16164,.T.);
#37592=EDGE_CURVE('',#29420,#29418,#1259,.T.);
#37593=EDGE_CURVE('',#29421,#29419,#16165,.T.);
#37594=EDGE_CURVE('',#29421,#29422,#16166,.T.);
#37595=EDGE_CURVE('',#29423,#29422,#16167,.T.);
#37596=EDGE_CURVE('',#29424,#29423,#16168,.T.);
#37597=EDGE_CURVE('',#29420,#29424,#16169,.T.);
#37598=EDGE_CURVE('',#29425,#29424,#1260,.T.);
#37599=EDGE_CURVE('',#29423,#29426,#601,.F.);
#37600=EDGE_CURVE('',#29426,#29425,#16170,.T.);
#37601=EDGE_CURVE('',#29422,#29427,#16171,.T.);
#37602=EDGE_CURVE('',#29428,#29421,#16172,.T.);
#37603=EDGE_CURVE('',#29427,#29428,#16173,.T.);
#37604=EDGE_CURVE('',#29426,#29429,#16174,.T.);
#37605=EDGE_CURVE('',#29429,#29430,#16175,.T.);
#37606=EDGE_CURVE('',#29430,#29431,#16176,.T.);
#37607=EDGE_CURVE('',#29432,#29431,#16177,.T.);
#37608=EDGE_CURVE('',#29433,#29432,#16178,.T.);
#37609=EDGE_CURVE('',#29425,#29433,#16179,.T.);
#37610=EDGE_CURVE('',#29434,#29433,#1261,.T.);
#37611=EDGE_CURVE('',#29432,#29435,#1262,.T.);
#37612=EDGE_CURVE('',#29435,#29434,#16180,.T.);
#37613=EDGE_CURVE('',#29431,#29436,#16181,.T.);
#37614=EDGE_CURVE('',#29436,#29437,#16182,.T.);
#37615=EDGE_CURVE('',#29428,#29437,#1263,.T.);
#37616=EDGE_CURVE('',#29413,#29435,#16183,.T.);
#37617=EDGE_CURVE('',#29438,#29438,#1264,.T.);
#37618=EDGE_CURVE('',#29439,#29427,#602,.T.);
#37619=EDGE_CURVE('',#29437,#29439,#16184,.T.);
#37620=EDGE_CURVE('',#29430,#29440,#16185,.T.);
#37621=EDGE_CURVE('',#29441,#29440,#16186,.T.);
#37622=EDGE_CURVE('',#29442,#29441,#16187,.T.);
#37623=EDGE_CURVE('',#29436,#29442,#16188,.T.);
#37624=EDGE_CURVE('',#29429,#29443,#16189,.T.);
#37625=EDGE_CURVE('',#29440,#29443,#16190,.T.);
#37626=EDGE_CURVE('',#29444,#29439,#16191,.T.);
#37627=EDGE_CURVE('',#29444,#29445,#16192,.T.);
#37628=EDGE_CURVE('',#29443,#29445,#16193,.T.);
#37629=EDGE_CURVE('',#29442,#29444,#16194,.T.);
#37630=EDGE_CURVE('',#29445,#29441,#16195,.T.);
#37631=EDGE_CURVE('',#29438,#29446,#16196,.T.);
#37632=EDGE_CURVE('',#29446,#29446,#1265,.T.);
#37633=EDGE_CURVE('',#29434,#29416,#16197,.T.);
#53501=ORIENTED_EDGE('',*,*,#37583,.T.);
#53502=ORIENTED_EDGE('',*,*,#37584,.T.);
#53503=ORIENTED_EDGE('',*,*,#37585,.T.);
#53504=ORIENTED_EDGE('',*,*,#37586,.T.);
#53505=ORIENTED_EDGE('',*,*,#37584,.F.);
#53506=ORIENTED_EDGE('',*,*,#37587,.T.);
#53507=ORIENTED_EDGE('',*,*,#37588,.F.);
#53508=ORIENTED_EDGE('',*,*,#37589,.F.);
#53509=ORIENTED_EDGE('',*,*,#37590,.T.);
#53510=ORIENTED_EDGE('',*,*,#37591,.T.);
#53511=ORIENTED_EDGE('',*,*,#37592,.T.);
#53512=ORIENTED_EDGE('',*,*,#37588,.T.);
#53513=ORIENTED_EDGE('',*,*,#37591,.F.);
#53514=ORIENTED_EDGE('',*,*,#37593,.F.);
#53515=ORIENTED_EDGE('',*,*,#37594,.T.);
#53516=ORIENTED_EDGE('',*,*,#37595,.F.);
#53517=ORIENTED_EDGE('',*,*,#37596,.F.);
#53518=ORIENTED_EDGE('',*,*,#37597,.F.);
#53519=ORIENTED_EDGE('',*,*,#37598,.T.);
#53520=ORIENTED_EDGE('',*,*,#37596,.T.);
#53521=ORIENTED_EDGE('',*,*,#37599,.T.);
#53522=ORIENTED_EDGE('',*,*,#37600,.T.);
#53523=ORIENTED_EDGE('',*,*,#37601,.F.);
#53524=ORIENTED_EDGE('',*,*,#37594,.F.);
#53525=ORIENTED_EDGE('',*,*,#37602,.F.);
#53526=ORIENTED_EDGE('',*,*,#37603,.F.);
#53527=ORIENTED_EDGE('',*,*,#37600,.F.);
#53528=ORIENTED_EDGE('',*,*,#37604,.T.);
#53529=ORIENTED_EDGE('',*,*,#37605,.T.);
#53530=ORIENTED_EDGE('',*,*,#37606,.T.);
#53531=ORIENTED_EDGE('',*,*,#37607,.F.);
#53532=ORIENTED_EDGE('',*,*,#37608,.F.);
#53533=ORIENTED_EDGE('',*,*,#37609,.F.);
#53534=ORIENTED_EDGE('',*,*,#37610,.T.);
#53535=ORIENTED_EDGE('',*,*,#37608,.T.);
#53536=ORIENTED_EDGE('',*,*,#37611,.T.);
#53537=ORIENTED_EDGE('',*,*,#37612,.T.);
#53538=ORIENTED_EDGE('',*,*,#37611,.F.);
#53539=ORIENTED_EDGE('',*,*,#37607,.T.);
#53540=ORIENTED_EDGE('',*,*,#37613,.T.);
#53541=ORIENTED_EDGE('',*,*,#37614,.T.);
#53542=ORIENTED_EDGE('',*,*,#37615,.F.);
#53543=ORIENTED_EDGE('',*,*,#37602,.T.);
#53544=ORIENTED_EDGE('',*,*,#37593,.T.);
#53545=ORIENTED_EDGE('',*,*,#37590,.F.);
#53546=ORIENTED_EDGE('',*,*,#37587,.F.);
#53547=ORIENTED_EDGE('',*,*,#37583,.F.);
#53548=ORIENTED_EDGE('',*,*,#37616,.T.);
#53549=ORIENTED_EDGE('',*,*,#37617,.T.);
#53550=ORIENTED_EDGE('',*,*,#37618,.T.);
#53551=ORIENTED_EDGE('',*,*,#37603,.T.);
#53552=ORIENTED_EDGE('',*,*,#37615,.T.);
#53553=ORIENTED_EDGE('',*,*,#37619,.T.);
#53554=ORIENTED_EDGE('',*,*,#37613,.F.);
#53555=ORIENTED_EDGE('',*,*,#37606,.F.);
#53556=ORIENTED_EDGE('',*,*,#37620,.T.);
#53557=ORIENTED_EDGE('',*,*,#37621,.F.);
#53558=ORIENTED_EDGE('',*,*,#37622,.F.);
#53559=ORIENTED_EDGE('',*,*,#37623,.F.);
#53560=ORIENTED_EDGE('',*,*,#37605,.F.);
#53561=ORIENTED_EDGE('',*,*,#37624,.T.);
#53562=ORIENTED_EDGE('',*,*,#37625,.F.);
#53563=ORIENTED_EDGE('',*,*,#37620,.F.);
#53564=ORIENTED_EDGE('',*,*,#37618,.F.);
#53565=ORIENTED_EDGE('',*,*,#37626,.F.);
#53566=ORIENTED_EDGE('',*,*,#37627,.T.);
#53567=ORIENTED_EDGE('',*,*,#37628,.F.);
#53568=ORIENTED_EDGE('',*,*,#37624,.F.);
#53569=ORIENTED_EDGE('',*,*,#37604,.F.);
#53570=ORIENTED_EDGE('',*,*,#37599,.F.);
#53571=ORIENTED_EDGE('',*,*,#37595,.T.);
#53572=ORIENTED_EDGE('',*,*,#37601,.T.);
#53573=ORIENTED_EDGE('',*,*,#37629,.F.);
#53574=ORIENTED_EDGE('',*,*,#37622,.T.);
#53575=ORIENTED_EDGE('',*,*,#37630,.F.);
#53576=ORIENTED_EDGE('',*,*,#37627,.F.);
#53577=ORIENTED_EDGE('',*,*,#37614,.F.);
#53578=ORIENTED_EDGE('',*,*,#37623,.T.);
#53579=ORIENTED_EDGE('',*,*,#37629,.T.);
#53580=ORIENTED_EDGE('',*,*,#37626,.T.);
#53581=ORIENTED_EDGE('',*,*,#37619,.F.);
#53582=ORIENTED_EDGE('',*,*,#37625,.T.);
#53583=ORIENTED_EDGE('',*,*,#37628,.T.);
#53584=ORIENTED_EDGE('',*,*,#37630,.T.);
#53585=ORIENTED_EDGE('',*,*,#37621,.T.);
#53586=ORIENTED_EDGE('',*,*,#37617,.F.);
#53587=ORIENTED_EDGE('',*,*,#37631,.T.);
#53588=ORIENTED_EDGE('',*,*,#37632,.F.);
#53589=ORIENTED_EDGE('',*,*,#37631,.F.);
#53590=ORIENTED_EDGE('',*,*,#37586,.F.);
#53591=ORIENTED_EDGE('',*,*,#37633,.F.);
#53592=ORIENTED_EDGE('',*,*,#37612,.F.);
#53593=ORIENTED_EDGE('',*,*,#37616,.F.);
#53594=ORIENTED_EDGE('',*,*,#37598,.F.);
#53595=ORIENTED_EDGE('',*,*,#37609,.T.);
#53596=ORIENTED_EDGE('',*,*,#37610,.F.);
#53597=ORIENTED_EDGE('',*,*,#37633,.T.);
#53598=ORIENTED_EDGE('',*,*,#37585,.F.);
#53599=ORIENTED_EDGE('',*,*,#37589,.T.);
#53600=ORIENTED_EDGE('',*,*,#37592,.F.);
#53601=ORIENTED_EDGE('',*,*,#37597,.T.);
#53602=ORIENTED_EDGE('',*,*,#37632,.T.);
#59849=ADVANCED_FACE('',(#6749),#707,.F.);
#59850=ADVANCED_FACE('',(#6750),#708,.T.);
#59851=ADVANCED_FACE('',(#6751),#709,.F.);
#59852=ADVANCED_FACE('',(#6752),#3696,.T.);
#59853=ADVANCED_FACE('',(#6753),#710,.T.);
#59854=ADVANCED_FACE('',(#6754),#3697,.T.);
#59855=ADVANCED_FACE('',(#6755),#3698,.T.);
#59856=ADVANCED_FACE('',(#6756),#711,.T.);
#59857=ADVANCED_FACE('',(#6757,#1847),#3699,.F.);
#59858=ADVANCED_FACE('',(#6758),#712,.F.);
#59859=ADVANCED_FACE('',(#6759),#3700,.T.);
#59860=ADVANCED_FACE('',(#6760),#3701,.T.);
#59861=ADVANCED_FACE('',(#6761),#3702,.T.);
#59862=ADVANCED_FACE('',(#6762),#3703,.T.);
#59863=ADVANCED_FACE('',(#6763),#3704,.T.);
#59864=ADVANCED_FACE('',(#6764),#3705,.T.);
#59865=ADVANCED_FACE('',(#6765),#713,.F.);
#59866=ADVANCED_FACE('',(#6766),#3706,.T.);
#59867=ADVANCED_FACE('',(#6767,#1848),#3707,.T.);
#60400=CLOSED_SHELL('',(#59849,#59850,#59851,#59852,#59853,#59854,#59855,
#59856,#59857,#59858,#59859,#59860,#59861,#59862,#59863,#59864,#59865,#59866,
#59867));
#62923=AXIS2_PLACEMENT_3D('',#102018,#73689,#73690);
#62924=AXIS2_PLACEMENT_3D('',#102019,#73691,#73692);
#62925=AXIS2_PLACEMENT_3D('',#102022,#73693,#73694);
#62926=AXIS2_PLACEMENT_3D('',#102026,#73696,#73697);
#62927=AXIS2_PLACEMENT_3D('',#102028,#73699,#73700);
#62928=AXIS2_PLACEMENT_3D('',#102030,#73701,#73702);
#62929=AXIS2_PLACEMENT_3D('',#102033,#73704,#73705);
#62930=AXIS2_PLACEMENT_3D('',#102034,#73706,#73707);
#62931=AXIS2_PLACEMENT_3D('',#102036,#73708,#73709);
#62932=AXIS2_PLACEMENT_3D('',#102039,#73711,#73712);
#62933=AXIS2_PLACEMENT_3D('',#102040,#73713,#73714);
#62934=AXIS2_PLACEMENT_3D('',#102050,#73720,#73721);
#62935=AXIS2_PLACEMENT_3D('',#102052,#73722,#73723);
#62936=AXIS2_PLACEMENT_3D('',#102054,#73724,#73725);
#62937=AXIS2_PLACEMENT_3D('',#102056,#73727,#73728);
#62938=AXIS2_PLACEMENT_3D('',#102062,#73732,#73733);
#62939=AXIS2_PLACEMENT_3D('',#102074,#73740,#73741);
#62940=AXIS2_PLACEMENT_3D('',#102076,#73742,#73743);
#62941=AXIS2_PLACEMENT_3D('',#102078,#73744,#73745);
#62942=AXIS2_PLACEMENT_3D('',#102080,#73747,#73748);
#62943=AXIS2_PLACEMENT_3D('',#102085,#73751,#73752);
#62944=AXIS2_PLACEMENT_3D('',#102088,#73754,#73755);
#62945=AXIS2_PLACEMENT_3D('',#102089,#73756,#73757);
#62946=AXIS2_PLACEMENT_3D('',#102091,#73758,#73759);
#62947=AXIS2_PLACEMENT_3D('',#102093,#73761,#73762);
#62948=AXIS2_PLACEMENT_3D('',#102101,#73767,#73768);
#62949=AXIS2_PLACEMENT_3D('',#102105,#73771,#73772);
#62950=AXIS2_PLACEMENT_3D('',#102111,#73776,#73777);
#62951=AXIS2_PLACEMENT_3D('',#102114,#73780,#73781);
#62952=AXIS2_PLACEMENT_3D('',#102115,#73782,#73783);
#62953=AXIS2_PLACEMENT_3D('',#102116,#73784,#73785);
#62954=AXIS2_PLACEMENT_3D('',#102119,#73787,#73788);
#62955=AXIS2_PLACEMENT_3D('',#102120,#73789,#73790);
#62956=AXIS2_PLACEMENT_3D('',#102122,#73792,#73793);
#73689=DIRECTION('axis',(0.,0.,1.));
#73690=DIRECTION('refdir',(1.,0.,0.));
#73691=DIRECTION('center_axis',(0.,0.,1.));
#73692=DIRECTION('ref_axis',(-0.0793928204885979,0.996843407990877,0.));
#73693=DIRECTION('center_axis',(0.,0.,-1.));
#73694=DIRECTION('ref_axis',(-0.0793928204885979,0.996843407990877,0.));
#73695=DIRECTION('',(0.,0.,1.));
#73696=DIRECTION('center_axis',(0.,0.,1.));
#73697=DIRECTION('ref_axis',(-0.0793928204885979,0.996843407990877,0.));
#73698=DIRECTION('',(0.,0.,-1.));
#73699=DIRECTION('center_axis',(0.,0.,1.));
#73700=DIRECTION('ref_axis',(1.,0.,0.));
#73701=DIRECTION('center_axis',(0.,0.,1.));
#73702=DIRECTION('ref_axis',(1.,0.,0.));
#73703=DIRECTION('',(0.,0.,-1.));
#73704=DIRECTION('center_axis',(0.,0.,1.));
#73705=DIRECTION('ref_axis',(1.,0.,0.));
#73706=DIRECTION('center_axis',(0.,0.,1.));
#73707=DIRECTION('ref_axis',(0.868164295052897,-0.496276895286599,0.));
#73708=DIRECTION('center_axis',(0.,0.,-1.));
#73709=DIRECTION('ref_axis',(0.868164295052897,-0.496276895286599,0.));
#73710=DIRECTION('',(0.,0.,1.));
#73711=DIRECTION('center_axis',(0.,0.,1.));
#73712=DIRECTION('ref_axis',(0.868164295052897,-0.496276895286599,0.));
#73713=DIRECTION('center_axis',(-0.535824439731477,0.844329420182933,0.));
#73714=DIRECTION('ref_axis',(-0.844329420182933,-0.535824439731477,0.));
#73715=DIRECTION('',(0.844329420182933,0.535824439731477,0.));
#73716=DIRECTION('',(0.,0.,1.));
#73717=DIRECTION('',(-0.612832075974817,-0.388912663599404,-0.687883556096824));
#73718=DIRECTION('',(0.,0.,-1.));
#73719=DIRECTION('',(-0.844329420182933,-0.535824439731477,0.));
#73720=DIRECTION('center_axis',(0.,0.,1.));
#73721=DIRECTION('ref_axis',(-0.975916153426266,0.21814596370706,0.));
#73722=DIRECTION('center_axis',(0.,0.,-1.));
#73723=DIRECTION('ref_axis',(-0.975916153426266,0.21814596370706,0.));
#73724=DIRECTION('center_axis',(0.746665039101869,0.,-0.665200209999218));
#73725=DIRECTION('ref_axis',(-0.665200209999218,0.,-0.746665039101869));
#73726=DIRECTION('',(0.,0.,1.));
#73727=DIRECTION('center_axis',(-0.844329420182933,-0.535824439731478,0.));
#73728=DIRECTION('ref_axis',(0.535824439731478,-0.844329420182933,0.));
#73729=DIRECTION('',(0.459172673933159,-0.723544819531037,0.51540600466319));
#73730=DIRECTION('',(-0.535824439731478,0.844329420182933,0.));
#73731=DIRECTION('',(0.,0.,-1.));
#73732=DIRECTION('center_axis',(-0.844329420182933,-0.535824439731478,0.));
#73733=DIRECTION('ref_axis',(0.535824439731478,-0.844329420182933,0.));
#73734=DIRECTION('',(0.459172673933159,-0.723544819531037,0.51540600466319));
#73735=DIRECTION('',(0.483554359415822,-0.76196444514008,-0.43079619988148));
#73736=DIRECTION('',(-0.459172673933159,0.723544819531037,-0.51540600466319));
#73737=DIRECTION('',(-0.535824439731478,0.844329420182933,0.));
#73738=DIRECTION('',(0.,0.,-1.));
#73739=DIRECTION('',(0.535824439731478,-0.844329420182933,0.));
#73740=DIRECTION('center_axis',(0.,0.,1.));
#73741=DIRECTION('ref_axis',(-0.218145963707059,-0.975916153426266,0.));
#73742=DIRECTION('center_axis',(0.,0.,-1.));
#73743=DIRECTION('ref_axis',(-0.218145963707059,-0.975916153426266,0.));
#73744=DIRECTION('center_axis',(0.,0.,1.));
#73745=DIRECTION('ref_axis',(-0.218145963707059,-0.975916153426266,0.));
#73746=DIRECTION('',(0.,0.,1.));
#73747=DIRECTION('center_axis',(0.,0.,1.));
#73748=DIRECTION('ref_axis',(1.,0.,0.));
#73749=DIRECTION('',(0.,1.,0.));
#73750=DIRECTION('',(-1.,0.,0.));
#73751=DIRECTION('center_axis',(0.,0.,-1.));
#73752=DIRECTION('ref_axis',(0.876306008119143,-0.481754896326226,0.));
#73753=DIRECTION('',(-0.844329420182934,-0.535824439731477,0.));
#73754=DIRECTION('center_axis',(0.,0.,1.));
#73755=DIRECTION('ref_axis',(1.,0.,0.));
#73756=DIRECTION('center_axis',(0.,0.,1.));
#73757=DIRECTION('ref_axis',(0.876306008119143,-0.481754896326226,0.));
#73758=DIRECTION('center_axis',(-0.746665039101869,0.,0.665200209999218));
#73759=DIRECTION('ref_axis',(0.665200209999218,0.,0.746665039101869));
#73760=DIRECTION('',(0.,0.,1.));
#73761=DIRECTION('center_axis',(0.746665039101869,0.,-0.665200209999218));
#73762=DIRECTION('ref_axis',(0.665200209999218,0.,0.746665039101869));
#73763=DIRECTION('',(0.,-1.,0.));
#73764=DIRECTION('',(0.665200209999218,0.,0.746665039101869));
#73765=DIRECTION('',(0.,-1.,0.));
#73766=DIRECTION('',(-0.665200209999218,0.,-0.746665039101869));
#73767=DIRECTION('center_axis',(0.665200209999218,0.,0.746665039101869));
#73768=DIRECTION('ref_axis',(-0.746665039101869,0.,0.665200209999218));
#73769=DIRECTION('',(0.,-1.,0.));
#73770=DIRECTION('',(-0.746665039101869,0.,0.665200209999218));
#73771=DIRECTION('center_axis',(-0.746665039101869,0.,0.665200209999218));
#73772=DIRECTION('ref_axis',(-0.665200209999218,0.,-0.746665039101869));
#73773=DIRECTION('',(0.665200209999218,0.,0.746665039101869));
#73774=DIRECTION('',(0.,-1.,0.));
#73775=DIRECTION('',(-0.665200209999218,0.,-0.746665039101869));
#73776=DIRECTION('center_axis',(-0.665200209999218,0.,-0.74666503910187));
#73777=DIRECTION('ref_axis',(0.74666503910187,0.,-0.665200209999218));
#73778=DIRECTION('',(-0.74666503910187,0.,0.665200209999218));
#73779=DIRECTION('',(0.74666503910187,0.,-0.665200209999218));
#73780=DIRECTION('center_axis',(0.,1.,0.));
#73781=DIRECTION('ref_axis',(1.,0.,0.));
#73782=DIRECTION('center_axis',(0.,-1.,0.));
#73783=DIRECTION('ref_axis',(0.,0.,-1.));
#73784=DIRECTION('center_axis',(0.,0.,1.));
#73785=DIRECTION('ref_axis',(1.,0.,0.));
#73786=DIRECTION('',(0.,0.,1.));
#73787=DIRECTION('center_axis',(0.,0.,-1.));
#73788=DIRECTION('ref_axis',(1.,0.,0.));
#73789=DIRECTION('center_axis',(0.535824439731477,-0.844329420182934,0.));
#73790=DIRECTION('ref_axis',(0.844329420182934,0.535824439731477,0.));
#73791=DIRECTION('',(0.844329420182934,0.535824439731477,0.));
#73792=DIRECTION('center_axis',(0.,0.,1.));
#73793=DIRECTION('ref_axis',(1.,0.,0.));
#102018=CARTESIAN_POINT('',(0.,0.,0.));
#102019=CARTESIAN_POINT('Origin',(107.825160250462,5.69826049129303,6.4));
#102020=CARTESIAN_POINT('',(107.557248030597,6.1204252013845,6.4));
#102021=CARTESIAN_POINT('',(108.022872954966,6.15750953753911,6.4));
#102022=CARTESIAN_POINT('Origin',(107.825160250462,5.69826049129303,6.4));
#102023=CARTESIAN_POINT('',(108.022872954966,6.15750953753911,8.4));
#102024=CARTESIAN_POINT('',(108.022872954966,6.15750953753911,6.4));
#102025=CARTESIAN_POINT('',(107.557248030597,6.1204252013845,8.4));
#102026=CARTESIAN_POINT('Origin',(107.825160250462,5.69826049129303,8.4));
#102027=CARTESIAN_POINT('',(107.557248030597,6.1204252013845,6.4));
#102028=CARTESIAN_POINT('Origin',(110.,10.75,6.4));
#102029=CARTESIAN_POINT('',(105.002771567388,10.9164571785702,6.4));
#102030=CARTESIAN_POINT('Origin',(110.,10.75,6.4));
#102031=CARTESIAN_POINT('',(105.002771567388,10.9164571785702,8.4));
#102032=CARTESIAN_POINT('',(105.002771567388,10.9164571785702,6.4));
#102033=CARTESIAN_POINT('Origin',(110.,10.75,8.4));
#102034=CARTESIAN_POINT('Origin',(104.503048724127,10.9331028964272,6.4));
#102035=CARTESIAN_POINT('',(104.770960943993,10.5109381863358,6.4));
#102036=CARTESIAN_POINT('Origin',(104.503048724127,10.9331028964272,6.4));
#102037=CARTESIAN_POINT('',(104.770960943993,10.5109381863358,8.4));
#102038=CARTESIAN_POINT('',(104.770960943993,10.5109381863358,6.4));
#102039=CARTESIAN_POINT('Origin',(104.503048724127,10.9331028964272,8.4));
#102040=CARTESIAN_POINT('Origin',(105.000867940784,10.6568407035301,6.4));
#102041=CARTESIAN_POINT('',(95.6068564566982,4.69525649247563,6.4));
#102042=CARTESIAN_POINT('',(95.6068564566982,4.69525649247563,6.4));
#102043=CARTESIAN_POINT('',(95.6068564566982,4.69525649247563,7.33954966094489));
#102044=CARTESIAN_POINT('',(95.6068564566982,4.69525649247563,6.4));
#102045=CARTESIAN_POINT('',(96.0290211667896,4.96316871234137,7.81341546108985));
#102046=CARTESIAN_POINT('',(98.0390228445825,6.23874670017144,10.0695752740066));
#102047=CARTESIAN_POINT('',(96.0290211667896,4.96316871234136,8.4));
#102048=CARTESIAN_POINT('',(96.0290211667896,4.96316871234137,6.4));
#102049=CARTESIAN_POINT('',(95.6068564566982,4.69525649247563,8.4));
#102050=CARTESIAN_POINT('Origin',(96.2969333866554,4.5410040022499,6.4));
#102051=CARTESIAN_POINT('',(95.8747686765639,4.27309178238416,8.4));
#102052=CARTESIAN_POINT('Origin',(96.2969333866554,4.5410040022499,8.4));
#102053=CARTESIAN_POINT('',(95.8747686765639,4.27309178238416,7.64027218795995));
#102054=CARTESIAN_POINT('Origin',(96.2969333866554,4.5410040022499,8.11413798810492));
#102055=CARTESIAN_POINT('',(95.8747686765639,4.27309178238416,6.4));
#102056=CARTESIAN_POINT('Origin',(95.6068564566982,4.69525649247563,6.4));
#102057=CARTESIAN_POINT('',(95.7511326297006,4.46791221986573,7.50149485088472));
#102058=CARTESIAN_POINT('',(95.8150253859024,4.36723272524474,7.57321233772642));
#102059=CARTESIAN_POINT('',(95.7511326297006,4.46791221986573,6.4));
#102060=CARTESIAN_POINT('',(98.3931435433018,0.304743507524373,6.4));
#102061=CARTESIAN_POINT('',(95.7511326297006,4.46791221986573,5.2163000524998));
#102062=CARTESIAN_POINT('Origin',(95.6068564566982,4.69525649247563,6.4));
#102063=CARTESIAN_POINT('',(96.2533349608981,3.67656309191811,8.06520020999922));
#102064=CARTESIAN_POINT('',(95.8150253859024,4.36723272524474,7.57321233772642));
#102065=CARTESIAN_POINT('',(97.7466650391019,1.32343690808192,6.73479979000078));
#102066=CARTESIAN_POINT('',(96.4723671690011,3.33142143066498,7.87006549336387));
#102067=CARTESIAN_POINT('',(97.4483935532906,1.79344046148143,6.4));
#102068=CARTESIAN_POINT('',(95.0971229410666,5.49847294134964,3.76077719575972));
#102069=CARTESIAN_POINT('',(98.1252313234361,0.726908217615838,6.4));
#102070=CARTESIAN_POINT('',(98.3931435433018,0.304743507524373,6.4));
#102071=CARTESIAN_POINT('',(98.1252313234361,0.726908217615838,8.4));
#102072=CARTESIAN_POINT('',(98.1252313234361,0.726908217615836,6.4));
#102073=CARTESIAN_POINT('',(98.3931435433018,0.304743507524373,8.4));
#102074=CARTESIAN_POINT('Origin',(98.5473960335276,0.99482043748158,6.4));
#102075=CARTESIAN_POINT('',(98.8153082533933,0.572655727390118,8.4));
#102076=CARTESIAN_POINT('Origin',(98.5473960335276,0.99482043748158,8.4));
#102077=CARTESIAN_POINT('',(98.8153082533933,0.572655727390118,6.4));
#102078=CARTESIAN_POINT('Origin',(98.5473960335276,0.99482043748158,6.4));
#102079=CARTESIAN_POINT('',(98.8153082533933,0.572655727390115,6.4));
#102080=CARTESIAN_POINT('Origin',(105.303428228349,8.02737175376219,6.4));
#102081=CARTESIAN_POINT('',(97.4483935532906,3.7,6.4));
#102082=CARTESIAN_POINT('',(97.4483935532906,5.86368587688109,6.4));
#102083=CARTESIAN_POINT('',(95.3289679196091,3.7,6.4));
#102084=CARTESIAN_POINT('',(99.6517141141745,3.7,6.4));
#102085=CARTESIAN_POINT('Origin',(95.3289679196091,4.2,6.4));
#102086=CARTESIAN_POINT('',(111.393143543302,8.55474350752437,6.4));
#102087=CARTESIAN_POINT('',(107.85,10.75,6.4));
#102088=CARTESIAN_POINT('Origin',(110.,10.75,6.4));
#102089=CARTESIAN_POINT('Origin',(95.3289679196091,4.2,5.2163000524998));
#102090=CARTESIAN_POINT('',(95.3289679196091,3.7,7.02762905073977));
#102091=CARTESIAN_POINT('Origin',(95.3289679196091,4.2,7.02762905073977));
#102092=CARTESIAN_POINT('',(95.3289679196091,3.7,5.2163000524998));
#102093=CARTESIAN_POINT('Origin',(91.7466650391019,3.7,0.));
#102094=CARTESIAN_POINT('',(97.7466650391019,0.6,6.73479979000078));
#102095=CARTESIAN_POINT('',(97.7466650391019,3.7,6.73479979000078));
#102096=CARTESIAN_POINT('',(91.7466650391019,0.6,0.));
#102097=CARTESIAN_POINT('',(97.7466650391019,0.6,6.73479979000078));
#102098=CARTESIAN_POINT('',(91.7466650391019,3.7,0.));
#102099=CARTESIAN_POINT('',(91.7466650391019,3.7,0.));
#102100=CARTESIAN_POINT('',(97.7466650391019,3.7,6.73479979000078));
#102101=CARTESIAN_POINT('Origin',(97.7466650391019,3.7,6.73479979000078));
#102102=CARTESIAN_POINT('',(96.2533349608981,0.6,8.06520020999922));
#102103=CARTESIAN_POINT('',(96.2533349608981,3.7,8.06520020999922));
#102104=CARTESIAN_POINT('',(96.2533349608981,0.6,8.06520020999922));
#102105=CARTESIAN_POINT('Origin',(96.2533349608981,3.7,8.06520020999922));
#102106=CARTESIAN_POINT('',(90.2533349608981,3.7,1.33040041999844));
#102107=CARTESIAN_POINT('',(90.2533349608981,3.7,1.33040041999844));
#102108=CARTESIAN_POINT('',(90.2533349608981,0.6,1.33040041999844));
#102109=CARTESIAN_POINT('',(90.2533349608981,3.7,1.33040041999844));
#102110=CARTESIAN_POINT('',(90.2533349608981,0.6,1.33040041999844));
#102111=CARTESIAN_POINT('Origin',(90.2533349608981,3.7,1.33040041999844));
#102112=CARTESIAN_POINT('',(91.7466650391019,3.7,0.));
#102113=CARTESIAN_POINT('',(91.7466650391019,0.6,0.));
#102114=CARTESIAN_POINT('Origin',(94.,3.7,4.03260010499961));
#102115=CARTESIAN_POINT('Origin',(94.,0.6,4.03260010499961));
#102116=CARTESIAN_POINT('Origin',(110.,10.75,6.4));
#102117=CARTESIAN_POINT('',(107.85,10.75,8.4));
#102118=CARTESIAN_POINT('',(107.85,10.75,6.4));
#102119=CARTESIAN_POINT('Origin',(110.,10.75,8.4));
#102120=CARTESIAN_POINT('Origin',(98.3931435433018,0.304743507524372,6.4));
#102121=CARTESIAN_POINT('',(111.393143543302,8.55474350752437,8.4));
#102122=CARTESIAN_POINT('Origin',(105.303428228349,8.02737175376219,8.4));
#113954=UNCERTAINTY_MEASURE_WITH_UNIT(LENGTH_MEASURE(0.01),#113985,
'DISTANCE_ACCURACY_VALUE',
'Maximum model space distance between geometric entities at asserted c
onnectivities');
#113964=UNCERTAINTY_MEASURE_WITH_UNIT(LENGTH_MEASURE(0.01),#113985,
'DISTANCE_ACCURACY_VALUE',
'Maximum model space distance between geometric entities at asserted c
onnectivities');
#113974=(
GEOMETRIC_REPRESENTATION_CONTEXT(3)
GLOBAL_UNCERTAINTY_ASSIGNED_CONTEXT((#113954))
GLOBAL_UNIT_ASSIGNED_CONTEXT((#113985,#113987,#113988))
REPRESENTATION_CONTEXT('','3D')
);
#113984=(
GEOMETRIC_REPRESENTATION_CONTEXT(3)
GLOBAL_UNCERTAINTY_ASSIGNED_CONTEXT((#113964))
GLOBAL_UNIT_ASSIGNED_CONTEXT((#113985,#113987,#113988))
REPRESENTATION_CONTEXT('','3D')
);
#113985=(
LENGTH_UNIT()
NAMED_UNIT(*)
SI_UNIT(.MILLI.,.METRE.)
);
#113987=(
NAMED_UNIT(*)
PLANE_ANGLE_UNIT()
SI_UNIT($,.RADIAN.)
);
#113988=(
NAMED_UNIT(*)
SI_UNIT($,.STERADIAN.)
SOLID_ANGLE_UNIT()
);
#113998=SHAPE_DEFINITION_REPRESENTATION(#114017,#114060);
#114017=PRODUCT_DEFINITION_SHAPE('',$,#114080);
#114060=SHAPE_REPRESENTATION('',(#62923),#113974);
#114070=PRODUCT_DEFINITION_CONTEXT('part definition',#114129,'design');
#114080=PRODUCT_DEFINITION('2026-10-05-09-50-45-275',
'Base Lock Knob Lever (stainless, bent)',#114099,#114070);
#114099=PRODUCT_DEFINITION_FORMATION('',$,#114140);
#114129=APPLICATION_CONTEXT(
'Core Data for Automotive Mechanical Design Process');
#114130=PRODUCT_CONTEXT('part definition',#114129,'mechanical');
#114140=PRODUCT('2026-10-05-09-50-45-275',
'Base Lock Knob Lever (stainless, bent)',$,(#114130));
#114283=COLOUR_RGB('Dark Blue',0.08,0.2,0.34);
#114284=FILL_AREA_STYLE_COLOUR('',#114283);
#114285=FILL_AREA_STYLE('',(#114284));
#114286=SURFACE_STYLE_FILL_AREA(#114285);
#114287=SURFACE_SIDE_STYLE('',(#114286));
#114288=SURFACE_STYLE_USAGE(.BOTH.,#114287);
#114289=PRESENTATION_STYLE_ASSIGNMENT((#114288));
ENDSEC;
END-ISO-10303-21;
